ISO-10303-21;
HEADER;
/* Generated by software containing ST-Developer
 * from STEP Tools, Inc. (www.steptools.com) 
 */

FILE_DESCRIPTION(
/* description */ (''),
/* implementation_level */ '2;1');

FILE_NAME(
/* name */ 'Clamp_03.step',
/* time_stamp */ '2026-10-22T13:39:42+06:00',
/* author */ (''),
/* organization */ (''),
/* preprocessor_version */ 'ST-DEVELOPER v20.2',
/* originating_system */ 'Autodesk Translation Framework v15.15.0.0',
/* authorisation */ '');

FILE_SCHEMA (('AUTOMOTIVE_DESIGN { 1 0 10303 214 3 1 1 }'));
ENDSEC;

DATA;
#10=MECHANICAL_DESIGN_GEOMETRIC_PRESENTATION_REPRESENTATION('',(#315),#17836);
#195=SPHERICAL_SURFACE('',#10848,0.299999999999994);
#196=SPHERICAL_SURFACE('',#10859,0.3);
#197=SPHERICAL_SURFACE('',#10863,0.299999999999994);
#198=SPHERICAL_SURFACE('',#10868,0.3);
#199=SPHERICAL_SURFACE('',#10872,0.300000000000011);
#200=SPHERICAL_SURFACE('',#10876,0.300000000000003);
#201=SPHERICAL_SURFACE('',#10880,0.299999999999994);
#202=SPHERICAL_SURFACE('',#10885,0.300000000000011);
#255=TOROIDAL_SURFACE('',#10830,4.79999999999999,0.3);
#256=TOROIDAL_SURFACE('',#10836,4.79999999999998,0.3);
#257=TOROIDAL_SURFACE('',#10843,0.600000000000001,0.3);
#258=TOROIDAL_SURFACE('',#10852,0.600000000000001,0.300000000000011);
#259=TOROIDAL_SURFACE('',#10915,4.79999999999998,0.3);
#260=TOROIDAL_SURFACE('',#10920,4.79999999999999,0.3);
#283=ELLIPSE('',#10858,0.424264068711946,0.3);
#284=ELLIPSE('',#10902,0.424264068711924,0.3);
#295=SHAPE_REPRESENTATION_RELATIONSHIP('SRR','None',#17882,#305);
#305=ADVANCED_BREP_SHAPE_REPRESENTATION('',(#325),#17834);
#315=STYLED_ITEM('',(#17987),#325);
#325=MANIFOLD_SOLID_BREP('Clamp_03',#9636);
#594=CYLINDRICAL_SURFACE('',#10827,0.3);
#595=CYLINDRICAL_SURFACE('',#10834,0.3);
#596=CYLINDRICAL_SURFACE('',#10839,4.49999999999999);
#597=CYLINDRICAL_SURFACE('',#10857,0.3);
#598=CYLINDRICAL_SURFACE('',#10867,0.3);
#599=CYLINDRICAL_SURFACE('',#10884,0.3);
#600=CYLINDRICAL_SURFACE('',#10889,0.3);
#601=CYLINDRICAL_SURFACE('',#10890,0.3);
#602=CYLINDRICAL_SURFACE('',#10891,0.3);
#603=CYLINDRICAL_SURFACE('',#10892,0.3);
#604=CYLINDRICAL_SURFACE('',#10893,0.3);
#605=CYLINDRICAL_SURFACE('',#10894,0.3);
#606=CYLINDRICAL_SURFACE('',#10895,0.3);
#607=CYLINDRICAL_SURFACE('',#10896,0.3);
#608=CYLINDRICAL_SURFACE('',#10897,0.3);
#609=CYLINDRICAL_SURFACE('',#10898,0.3);
#610=CYLINDRICAL_SURFACE('',#10899,0.3);
#611=CYLINDRICAL_SURFACE('',#10900,0.3);
#612=CYLINDRICAL_SURFACE('',#10901,0.3);
#613=CYLINDRICAL_SURFACE('',#10903,0.3);
#614=CYLINDRICAL_SURFACE('',#10912,0.3);
#615=CYLINDRICAL_SURFACE('',#10918,0.3);
#616=CYLINDRICAL_SURFACE('',#10921,4.49999999999998);
#1211=LINE('',#17415,#1876);
#1212=LINE('',#17418,#1877);
#1213=LINE('',#17429,#1878);
#1214=LINE('',#17430,#1879);
#1215=LINE('',#17436,#1880);
#1216=LINE('',#17439,#1881);
#1217=LINE('',#17442,#1882);
#1218=LINE('',#17443,#1883);
#1219=LINE('',#17447,#1884);
#1220=LINE('',#17449,#1885);
#1221=LINE('',#17451,#1886);
#1222=LINE('',#17452,#1887);
#1223=LINE('',#17478,#1888);
#1224=LINE('',#17481,#1889);
#1225=LINE('',#17496,#1890);
#1226=LINE('',#17497,#1891);
#1227=LINE('',#17526,#1892);
#1228=LINE('',#17527,#1893);
#1229=LINE('',#17536,#1894);
#1230=LINE('',#17537,#1895);
#1231=LINE('',#17539,#1896);
#1232=LINE('',#17540,#1897);
#1233=LINE('',#17542,#1898);
#1234=LINE('',#17543,#1899);
#1235=LINE('',#17545,#1900);
#1236=LINE('',#17546,#1901);
#1237=LINE('',#17548,#1902);
#1238=LINE('',#17549,#1903);
#1239=LINE('',#17551,#1904);
#1240=LINE('',#17552,#1905);
#1241=LINE('',#17554,#1906);
#1242=LINE('',#17556,#1907);
#1243=LINE('',#17558,#1908);
#1244=LINE('',#17559,#1909);
#1245=LINE('',#17561,#1910);
#1246=LINE('',#17562,#1911);
#1247=LINE('',#17564,#1912);
#1248=LINE('',#17566,#1913);
#1249=LINE('',#17569,#1914);
#1250=LINE('',#17572,#1915);
#1251=LINE('',#17574,#1916);
#1252=LINE('',#17575,#1917);
#1253=LINE('',#17577,#1918);
#1254=LINE('',#17583,#1919);
#1255=LINE('',#17587,#1920);
#1256=LINE('',#17600,#1921);
#1257=LINE('',#17603,#1922);
#1876=VECTOR('',#13763,10.);
#1877=VECTOR('',#13766,10.);
#1878=VECTOR('',#13779,10.);
#1879=VECTOR('',#13780,10.);
#1880=VECTOR('',#13789,10.);
#1881=VECTOR('',#13792,10.);
#1882=VECTOR('',#13795,10.);
#1883=VECTOR('',#13796,10.);
#1884=VECTOR('',#13799,10.);
#1885=VECTOR('',#13800,10.);
#1886=VECTOR('',#13801,10.);
#1887=VECTOR('',#13802,10.);
#1888=VECTOR('',#13833,10.);
#1889=VECTOR('',#13836,10.);
#1890=VECTOR('',#13855,10.);
#1891=VECTOR('',#13856,10.);
#1892=VECTOR('',#13891,10.);
#1893=VECTOR('',#13892,10.);
#1894=VECTOR('',#13903,10.);
#1895=VECTOR('',#13904,10.);
#1896=VECTOR('',#13907,10.);
#1897=VECTOR('',#13908,10.);
#1898=VECTOR('',#13911,10.);
#1899=VECTOR('',#13912,10.);
#1900=VECTOR('',#13915,10.);
#1901=VECTOR('',#13916,10.);
#1902=VECTOR('',#13919,10.);
#1903=VECTOR('',#13920,10.);
#1904=VECTOR('',#13923,10.);
#1905=VECTOR('',#13924,10.);
#1906=VECTOR('',#13927,10.);
#1907=VECTOR('',#13930,10.);
#1908=VECTOR('',#13933,10.);
#1909=VECTOR('',#13934,10.);
#1910=VECTOR('',#13937,10.);
#1911=VECTOR('',#13938,10.);
#1912=VECTOR('',#13941,10.);
#1913=VECTOR('',#13944,10.);
#1914=VECTOR('',#13947,10.);
#1915=VECTOR('',#13950,10.);
#1916=VECTOR('',#13953,10.);
#1917=VECTOR('',#13954,10.);
#1918=VECTOR('',#13957,10.);
#1919=VECTOR('',#13964,10.);
#1920=VECTOR('',#13967,10.);
#1921=VECTOR('',#13990,10.);
#1922=VECTOR('',#13995,10.);
#2023=FACE_BOUND('',#3217,.T.);
#2024=FACE_BOUND('',#3249,.T.);
#2547=FACE_OUTER_BOUND('',#3210,.T.);
#2548=FACE_OUTER_BOUND('',#3211,.T.);
#2549=FACE_OUTER_BOUND('',#3212,.T.);
#2550=FACE_OUTER_BOUND('',#3213,.T.);
#2551=FACE_OUTER_BOUND('',#3214,.T.);
#2552=FACE_OUTER_BOUND('',#3215,.T.);
#2553=FACE_OUTER_BOUND('',#3216,.T.);
#2554=FACE_OUTER_BOUND('',#3218,.T.);
#2555=FACE_OUTER_BOUND('',#3219,.T.);
#2556=FACE_OUTER_BOUND('',#3220,.T.);
#2557=FACE_OUTER_BOUND('',#3221,.T.);
#2558=FACE_OUTER_BOUND('',#3222,.T.);
#2559=FACE_OUTER_BOUND('',#3223,.T.);
#2560=FACE_OUTER_BOUND('',#3224,.T.);
#2561=FACE_OUTER_BOUND('',#3225,.T.);
#2562=FACE_OUTER_BOUND('',#3226,.T.);
#2563=FACE_OUTER_BOUND('',#3227,.T.);
#2564=FACE_OUTER_BOUND('',#3228,.T.);
#2565=FACE_OUTER_BOUND('',#3229,.T.);
#2566=FACE_OUTER_BOUND('',#3230,.T.);
#2567=FACE_OUTER_BOUND('',#3231,.T.);
#2568=FACE_OUTER_BOUND('',#3232,.T.);
#2569=FACE_OUTER_BOUND('',#3233,.T.);
#2570=FACE_OUTER_BOUND('',#3234,.T.);
#2571=FACE_OUTER_BOUND('',#3235,.T.);
#2572=FACE_OUTER_BOUND('',#3236,.T.);
#2573=FACE_OUTER_BOUND('',#3237,.T.);
#2574=FACE_OUTER_BOUND('',#3238,.T.);
#2575=FACE_OUTER_BOUND('',#3239,.T.);
#2576=FACE_OUTER_BOUND('',#3240,.T.);
#2577=FACE_OUTER_BOUND('',#3241,.T.);
#2578=FACE_OUTER_BOUND('',#3242,.T.);
#2579=FACE_OUTER_BOUND('',#3243,.T.);
#2580=FACE_OUTER_BOUND('',#3244,.T.);
#2581=FACE_OUTER_BOUND('',#3245,.T.);
#2582=FACE_OUTER_BOUND('',#3246,.T.);
#2583=FACE_OUTER_BOUND('',#3247,.T.);
#2584=FACE_OUTER_BOUND('',#3248,.T.);
#2585=FACE_OUTER_BOUND('',#3250,.T.);
#2586=FACE_OUTER_BOUND('',#3251,.T.);
#2587=FACE_OUTER_BOUND('',#3252,.T.);
#2588=FACE_OUTER_BOUND('',#3253,.T.);
#2589=FACE_OUTER_BOUND('',#3254,.T.);
#2590=FACE_OUTER_BOUND('',#3255,.T.);
#2591=FACE_OUTER_BOUND('',#3256,.T.);
#2592=FACE_OUTER_BOUND('',#3257,.T.);
#2593=FACE_OUTER_BOUND('',#3258,.T.);
#3210=EDGE_LOOP('',(#8477,#8478,#8479,#8480));
#3211=EDGE_LOOP('',(#8481,#8482,#8483,#8484));
#3212=EDGE_LOOP('',(#8485,#8486,#8487,#8488));
#3213=EDGE_LOOP('',(#8489,#8490,#8491,#8492));
#3214=EDGE_LOOP('',(#8493,#8494,#8495,#8496));
#3215=EDGE_LOOP('',(#8497,#8498,#8499,#8500));
#3216=EDGE_LOOP('',(#8501,#8502,#8503,#8504));
#3217=EDGE_LOOP('',(#8505,#8506,#8507,#8508));
#3218=EDGE_LOOP('',(#8509,#8510,#8511,#8512));
#3219=EDGE_LOOP('',(#8513,#8514,#8515));
#3220=EDGE_LOOP('',(#8516,#8517,#8518,#8519));
#3221=EDGE_LOOP('',(#8520,#8521,#8522,#8523));
#3222=EDGE_LOOP('',(#8524,#8525,#8526));
#3223=EDGE_LOOP('',(#8527,#8528,#8529));
#3224=EDGE_LOOP('',(#8530,#8531,#8532,#8533));
#3225=EDGE_LOOP('',(#8534,#8535,#8536));
#3226=EDGE_LOOP('',(#8537,#8538,#8539));
#3227=EDGE_LOOP('',(#8540,#8541,#8542));
#3228=EDGE_LOOP('',(#8543,#8544,#8545));
#3229=EDGE_LOOP('',(#8546,#8547,#8548,#8549));
#3230=EDGE_LOOP('',(#8550,#8551,#8552));
#3231=EDGE_LOOP('',(#8553,#8554,#8555,#8556));
#3232=EDGE_LOOP('',(#8557,#8558,#8559,#8560));
#3233=EDGE_LOOP('',(#8561,#8562,#8563,#8564));
#3234=EDGE_LOOP('',(#8565,#8566,#8567,#8568));
#3235=EDGE_LOOP('',(#8569,#8570,#8571,#8572));
#3236=EDGE_LOOP('',(#8573,#8574,#8575,#8576));
#3237=EDGE_LOOP('',(#8577,#8578,#8579,#8580));
#3238=EDGE_LOOP('',(#8581,#8582,#8583,#8584));
#3239=EDGE_LOOP('',(#8585,#8586,#8587,#8588));
#3240=EDGE_LOOP('',(#8589,#8590,#8591,#8592));
#3241=EDGE_LOOP('',(#8593,#8594,#8595,#8596));
#3242=EDGE_LOOP('',(#8597,#8598,#8599,#8600));
#3243=EDGE_LOOP('',(#8601,#8602,#8603,#8604));
#3244=EDGE_LOOP('',(#8605,#8606,#8607,#8608));
#3245=EDGE_LOOP('',(#8609,#8610,#8611,#8612));
#3246=EDGE_LOOP('',(#8613,#8614,#8615,#8616,#8617,#8618,#8619));
#3247=EDGE_LOOP('',(#8620,#8621,#8622,#8623));
#3248=EDGE_LOOP('',(#8624,#8625,#8626,#8627));
#3249=EDGE_LOOP('',(#8628,#8629,#8630,#8631));
#3250=EDGE_LOOP('',(#8632,#8633,#8634,#8635));
#3251=EDGE_LOOP('',(#8636,#8637,#8638,#8639,#8640,#8641,#8642));
#3252=EDGE_LOOP('',(#8643,#8644,#8645,#8646));
#3253=EDGE_LOOP('',(#8647,#8648,#8649,#8650));
#3254=EDGE_LOOP('',(#8651,#8652,#8653,#8654));
#3255=EDGE_LOOP('',(#8655,#8656,#8657,#8658));
#3256=EDGE_LOOP('',(#8659,#8660,#8661,#8662));
#3257=EDGE_LOOP('',(#8663,#8664,#8665,#8666));
#3258=EDGE_LOOP('',(#8667,#8668,#8669,#8670));
#3840=CIRCLE('',#10828,0.3);
#3841=CIRCLE('',#10829,0.299999999999994);
#3842=CIRCLE('',#10831,0.300000000000011);
#3843=CIRCLE('',#10832,4.49999999999999);
#3844=CIRCLE('',#10833,4.79999999999999);
#3845=CIRCLE('',#10835,0.300000000000002);
#3846=CIRCLE('',#10837,4.49999999999998);
#3847=CIRCLE('',#10838,4.79999999999998);
#3848=CIRCLE('',#10840,4.49999999999999);
#3849=CIRCLE('',#10844,0.3);
#3850=CIRCLE('',#10845,0.599999999999987);
#3851=CIRCLE('',#10846,0.300000000000011);
#3852=CIRCLE('',#10847,0.299999999999994);
#3853=CIRCLE('',#10849,0.3);
#3854=CIRCLE('',#10850,0.300000000000011);
#3855=CIRCLE('',#10851,0.299999999999994);
#3856=CIRCLE('',#10853,0.600000000000001);
#3857=CIRCLE('',#10854,0.300000000000011);
#3858=CIRCLE('',#10855,0.3);
#3859=CIRCLE('',#10856,0.299999999999976);
#3860=CIRCLE('',#10860,0.300000000000003);
#3861=CIRCLE('',#10861,0.300000000000011);
#3862=CIRCLE('',#10862,0.3);
#3863=CIRCLE('',#10864,0.3);
#3864=CIRCLE('',#10865,0.300000000000011);
#3865=CIRCLE('',#10866,0.299999999999994);
#3866=CIRCLE('',#10869,0.299999999999994);
#3867=CIRCLE('',#10870,0.300000000000011);
#3868=CIRCLE('',#10871,0.3);
#3869=CIRCLE('',#10873,0.300000000000006);
#3870=CIRCLE('',#10874,0.3);
#3871=CIRCLE('',#10875,0.300000000000011);
#3872=CIRCLE('',#10877,0.3);
#3873=CIRCLE('',#10878,0.300000000000011);
#3874=CIRCLE('',#10879,0.300000000000003);
#3875=CIRCLE('',#10881,0.300000000000011);
#3876=CIRCLE('',#10882,0.3);
#3877=CIRCLE('',#10883,0.299999999999994);
#3878=CIRCLE('',#10886,0.3);
#3879=CIRCLE('',#10887,0.300000000000001);
#3880=CIRCLE('',#10888,0.300000000000011);
#3881=CIRCLE('',#10908,4.79999999999999);
#3882=CIRCLE('',#10909,4.79999999999998);
#3883=CIRCLE('',#10913,0.3);
#3884=CIRCLE('',#10914,0.299999999999994);
#3885=CIRCLE('',#10916,0.300000000000002);
#3886=CIRCLE('',#10917,4.49999999999998);
#3887=CIRCLE('',#10919,0.300000000000002);
#4618=VERTEX_POINT('',#17411);
#4619=VERTEX_POINT('',#17412);
#4620=VERTEX_POINT('',#17414);
#4621=VERTEX_POINT('',#17416);
#4622=VERTEX_POINT('',#17420);
#4623=VERTEX_POINT('',#17421);
#4624=VERTEX_POINT('',#17426);
#4625=VERTEX_POINT('',#17427);
#4626=VERTEX_POINT('',#17435);
#4627=VERTEX_POINT('',#17437);
#4628=VERTEX_POINT('',#17441);
#4629=VERTEX_POINT('',#17445);
#4630=VERTEX_POINT('',#17446);
#4631=VERTEX_POINT('',#17448);
#4632=VERTEX_POINT('',#17450);
#4633=VERTEX_POINT('',#17454);
#4634=VERTEX_POINT('',#17456);
#4635=VERTEX_POINT('',#17458);
#4636=VERTEX_POINT('',#17462);
#4637=VERTEX_POINT('',#17463);
#4638=VERTEX_POINT('',#17465);
#4639=VERTEX_POINT('',#17469);
#4640=VERTEX_POINT('',#17470);
#4641=VERTEX_POINT('',#17473);
#4642=VERTEX_POINT('',#17477);
#4643=VERTEX_POINT('',#17479);
#4644=VERTEX_POINT('',#17483);
#4645=VERTEX_POINT('',#17484);
#4646=VERTEX_POINT('',#17489);
#4647=VERTEX_POINT('',#17490);
#4648=VERTEX_POINT('',#17492);
#4649=VERTEX_POINT('',#17499);
#4650=VERTEX_POINT('',#17500);
#4651=VERTEX_POINT('',#17502);
#4652=VERTEX_POINT('',#17506);
#4653=VERTEX_POINT('',#17508);
#4654=VERTEX_POINT('',#17512);
#4655=VERTEX_POINT('',#17513);
#4656=VERTEX_POINT('',#17515);
#4657=VERTEX_POINT('',#17519);
#4658=VERTEX_POINT('',#17520);
#4659=VERTEX_POINT('',#17522);
#4660=VERTEX_POINT('',#17529);
#4661=VERTEX_POINT('',#17530);
#4662=VERTEX_POINT('',#17532);
#4663=VERTEX_POINT('',#17568);
#4664=VERTEX_POINT('',#17570);
#4665=VERTEX_POINT('',#17581);
#4666=VERTEX_POINT('',#17582);
#4667=VERTEX_POINT('',#17584);
#4668=VERTEX_POINT('',#17586);
#4669=VERTEX_POINT('',#17595);
#5909=EDGE_CURVE('',#4618,#4619,#3840,.T.);
#5910=EDGE_CURVE('',#4620,#4618,#1211,.T.);
#5911=EDGE_CURVE('',#4621,#4620,#3841,.T.);
#5912=EDGE_CURVE('',#4619,#4621,#1212,.T.);
#5913=EDGE_CURVE('',#4622,#4623,#3842,.T.);
#5914=EDGE_CURVE('',#4621,#4622,#3843,.T.);
#5915=EDGE_CURVE('',#4623,#4620,#3844,.T.);
#5916=EDGE_CURVE('',#4624,#4625,#3845,.T.);
#5917=EDGE_CURVE('',#4622,#4624,#1213,.T.);
#5918=EDGE_CURVE('',#4625,#4623,#1214,.T.);
#5919=EDGE_CURVE('',#4624,#4619,#3846,.T.);
#5920=EDGE_CURVE('',#4618,#4625,#3847,.T.);
#5921=EDGE_CURVE('',#4626,#4622,#1215,.T.);
#5922=EDGE_CURVE('',#4626,#4627,#3848,.T.);
#5923=EDGE_CURVE('',#4627,#4621,#1216,.T.);
#5924=EDGE_CURVE('',#4627,#4628,#1217,.T.);
#5925=EDGE_CURVE('',#4628,#4619,#1218,.T.);
#5926=EDGE_CURVE('',#4629,#4630,#1219,.T.);
#5927=EDGE_CURVE('',#4630,#4631,#1220,.T.);
#5928=EDGE_CURVE('',#4631,#4632,#1221,.T.);
#5929=EDGE_CURVE('',#4632,#4629,#1222,.T.);
#5930=EDGE_CURVE('',#4632,#4633,#3849,.T.);
#5931=EDGE_CURVE('',#4634,#4633,#3850,.T.);
#5932=EDGE_CURVE('',#4634,#4635,#3851,.T.);
#5933=EDGE_CURVE('',#4635,#4632,#3852,.F.);
#5934=EDGE_CURVE('',#4636,#4637,#3853,.F.);
#5935=EDGE_CURVE('',#4637,#4638,#3854,.F.);
#5936=EDGE_CURVE('',#4638,#4636,#3855,.F.);
#5937=EDGE_CURVE('',#4639,#4640,#3856,.T.);
#5938=EDGE_CURVE('',#4639,#4629,#3857,.T.);
#5939=EDGE_CURVE('',#4629,#4641,#3858,.F.);
#5940=EDGE_CURVE('',#4641,#4640,#3859,.T.);
#5941=EDGE_CURVE('',#4642,#4641,#1223,.T.);
#5942=EDGE_CURVE('',#4643,#4642,#283,.T.);
#5943=EDGE_CURVE('',#4640,#4643,#1224,.T.);
#5944=EDGE_CURVE('',#4644,#4645,#3860,.F.);
#5945=EDGE_CURVE('',#4645,#4631,#3861,.F.);
#5946=EDGE_CURVE('',#4631,#4644,#3862,.F.);
#5947=EDGE_CURVE('',#4646,#4647,#3863,.F.);
#5948=EDGE_CURVE('',#4647,#4648,#3864,.F.);
#5949=EDGE_CURVE('',#4648,#4646,#3865,.F.);
#5950=EDGE_CURVE('',#4643,#4648,#1225,.T.);
#5951=EDGE_CURVE('',#4646,#4642,#1226,.T.);
#5952=EDGE_CURVE('',#4649,#4650,#3866,.F.);
#5953=EDGE_CURVE('',#4650,#4651,#3867,.F.);
#5954=EDGE_CURVE('',#4651,#4649,#3868,.F.);
#5955=EDGE_CURVE('',#4652,#4630,#3869,.F.);
#5956=EDGE_CURVE('',#4630,#4653,#3870,.F.);
#5957=EDGE_CURVE('',#4653,#4652,#3871,.F.);
#5958=EDGE_CURVE('',#4654,#4655,#3872,.F.);
#5959=EDGE_CURVE('',#4655,#4656,#3873,.F.);
#5960=EDGE_CURVE('',#4656,#4654,#3874,.F.);
#5961=EDGE_CURVE('',#4657,#4658,#3875,.F.);
#5962=EDGE_CURVE('',#4658,#4659,#3876,.F.);
#5963=EDGE_CURVE('',#4659,#4657,#3877,.F.);
#5964=EDGE_CURVE('',#4648,#4659,#1227,.T.);
#5965=EDGE_CURVE('',#4657,#4647,#1228,.T.);
#5966=EDGE_CURVE('',#4660,#4661,#3878,.F.);
#5967=EDGE_CURVE('',#4661,#4662,#3879,.F.);
#5968=EDGE_CURVE('',#4662,#4660,#3880,.F.);
#5969=EDGE_CURVE('',#4660,#4658,#1229,.T.);
#5970=EDGE_CURVE('',#4659,#4662,#1230,.T.);
#5971=EDGE_CURVE('',#4652,#4661,#1231,.T.);
#5972=EDGE_CURVE('',#4662,#4653,#1232,.T.);
#5973=EDGE_CURVE('',#4661,#4656,#1233,.T.);
#5974=EDGE_CURVE('',#4654,#4660,#1234,.T.);
#5975=EDGE_CURVE('',#4658,#4651,#1235,.T.);
#5976=EDGE_CURVE('',#4649,#4657,#1236,.T.);
#5977=EDGE_CURVE('',#4656,#4644,#1237,.T.);
#5978=EDGE_CURVE('',#4645,#4655,#1238,.T.);
#5979=EDGE_CURVE('',#4651,#4654,#1239,.T.);
#5980=EDGE_CURVE('',#4655,#4650,#1240,.T.);
#5981=EDGE_CURVE('',#4653,#4639,#1241,.T.);
#5982=EDGE_CURVE('',#4644,#4652,#1242,.T.);
#5983=EDGE_CURVE('',#4638,#4649,#1243,.T.);
#5984=EDGE_CURVE('',#4650,#4637,#1244,.T.);
#5985=EDGE_CURVE('',#4647,#4638,#1245,.T.);
#5986=EDGE_CURVE('',#4636,#4646,#1246,.T.);
#5987=EDGE_CURVE('',#4633,#4645,#1247,.T.);
#5988=EDGE_CURVE('',#4641,#4635,#1248,.T.);
#5989=EDGE_CURVE('',#4663,#4636,#1249,.T.);
#5990=EDGE_CURVE('',#4664,#4663,#284,.T.);
#5991=EDGE_CURVE('',#4637,#4664,#1250,.T.);
#5992=EDGE_CURVE('',#4664,#4634,#1251,.T.);
#5993=EDGE_CURVE('',#4635,#4663,#1252,.T.);
#5994=EDGE_CURVE('',#4642,#4663,#1253,.T.);
#5995=EDGE_CURVE('',#4665,#4666,#1254,.T.);
#5996=EDGE_CURVE('',#4666,#4667,#3881,.T.);
#5997=EDGE_CURVE('',#4667,#4668,#1255,.T.);
#5998=EDGE_CURVE('',#4668,#4665,#3882,.T.);
#5999=EDGE_CURVE('',#4666,#4627,#3883,.T.);
#6000=EDGE_CURVE('',#4628,#4665,#3884,.T.);
#6001=EDGE_CURVE('',#4669,#4668,#3885,.T.);
#6002=EDGE_CURVE('',#4628,#4669,#3886,.T.);
#6003=EDGE_CURVE('',#4626,#4667,#3887,.T.);
#6004=EDGE_CURVE('',#4669,#4626,#1256,.T.);
#6005=EDGE_CURVE('',#4669,#4624,#1257,.T.);
#8477=ORIENTED_EDGE('',*,*,#5909,.F.);
#8478=ORIENTED_EDGE('',*,*,#5910,.F.);
#8479=ORIENTED_EDGE('',*,*,#5911,.F.);
#8480=ORIENTED_EDGE('',*,*,#5912,.F.);
#8481=ORIENTED_EDGE('',*,*,#5913,.F.);
#8482=ORIENTED_EDGE('',*,*,#5914,.F.);
#8483=ORIENTED_EDGE('',*,*,#5911,.T.);
#8484=ORIENTED_EDGE('',*,*,#5915,.F.);
#8485=ORIENTED_EDGE('',*,*,#5916,.F.);
#8486=ORIENTED_EDGE('',*,*,#5917,.F.);
#8487=ORIENTED_EDGE('',*,*,#5913,.T.);
#8488=ORIENTED_EDGE('',*,*,#5918,.F.);
#8489=ORIENTED_EDGE('',*,*,#5909,.T.);
#8490=ORIENTED_EDGE('',*,*,#5919,.F.);
#8491=ORIENTED_EDGE('',*,*,#5916,.T.);
#8492=ORIENTED_EDGE('',*,*,#5920,.F.);
#8493=ORIENTED_EDGE('',*,*,#5914,.T.);
#8494=ORIENTED_EDGE('',*,*,#5921,.F.);
#8495=ORIENTED_EDGE('',*,*,#5922,.T.);
#8496=ORIENTED_EDGE('',*,*,#5923,.T.);
#8497=ORIENTED_EDGE('',*,*,#5912,.T.);
#8498=ORIENTED_EDGE('',*,*,#5923,.F.);
#8499=ORIENTED_EDGE('',*,*,#5924,.T.);
#8500=ORIENTED_EDGE('',*,*,#5925,.T.);
#8501=ORIENTED_EDGE('',*,*,#5926,.T.);
#8502=ORIENTED_EDGE('',*,*,#5927,.T.);
#8503=ORIENTED_EDGE('',*,*,#5928,.T.);
#8504=ORIENTED_EDGE('',*,*,#5929,.T.);
#8505=ORIENTED_EDGE('',*,*,#5910,.T.);
#8506=ORIENTED_EDGE('',*,*,#5920,.T.);
#8507=ORIENTED_EDGE('',*,*,#5918,.T.);
#8508=ORIENTED_EDGE('',*,*,#5915,.T.);
#8509=ORIENTED_EDGE('',*,*,#5930,.T.);
#8510=ORIENTED_EDGE('',*,*,#5931,.F.);
#8511=ORIENTED_EDGE('',*,*,#5932,.T.);
#8512=ORIENTED_EDGE('',*,*,#5933,.T.);
#8513=ORIENTED_EDGE('',*,*,#5934,.T.);
#8514=ORIENTED_EDGE('',*,*,#5935,.T.);
#8515=ORIENTED_EDGE('',*,*,#5936,.T.);
#8516=ORIENTED_EDGE('',*,*,#5937,.F.);
#8517=ORIENTED_EDGE('',*,*,#5938,.T.);
#8518=ORIENTED_EDGE('',*,*,#5939,.T.);
#8519=ORIENTED_EDGE('',*,*,#5940,.T.);
#8520=ORIENTED_EDGE('',*,*,#5941,.F.);
#8521=ORIENTED_EDGE('',*,*,#5942,.F.);
#8522=ORIENTED_EDGE('',*,*,#5943,.F.);
#8523=ORIENTED_EDGE('',*,*,#5940,.F.);
#8524=ORIENTED_EDGE('',*,*,#5944,.T.);
#8525=ORIENTED_EDGE('',*,*,#5945,.T.);
#8526=ORIENTED_EDGE('',*,*,#5946,.T.);
#8527=ORIENTED_EDGE('',*,*,#5947,.T.);
#8528=ORIENTED_EDGE('',*,*,#5948,.T.);
#8529=ORIENTED_EDGE('',*,*,#5949,.T.);
#8530=ORIENTED_EDGE('',*,*,#5950,.F.);
#8531=ORIENTED_EDGE('',*,*,#5942,.T.);
#8532=ORIENTED_EDGE('',*,*,#5951,.F.);
#8533=ORIENTED_EDGE('',*,*,#5949,.F.);
#8534=ORIENTED_EDGE('',*,*,#5952,.T.);
#8535=ORIENTED_EDGE('',*,*,#5953,.T.);
#8536=ORIENTED_EDGE('',*,*,#5954,.T.);
#8537=ORIENTED_EDGE('',*,*,#5955,.T.);
#8538=ORIENTED_EDGE('',*,*,#5956,.T.);
#8539=ORIENTED_EDGE('',*,*,#5957,.T.);
#8540=ORIENTED_EDGE('',*,*,#5958,.T.);
#8541=ORIENTED_EDGE('',*,*,#5959,.T.);
#8542=ORIENTED_EDGE('',*,*,#5960,.T.);
#8543=ORIENTED_EDGE('',*,*,#5961,.T.);
#8544=ORIENTED_EDGE('',*,*,#5962,.T.);
#8545=ORIENTED_EDGE('',*,*,#5963,.T.);
#8546=ORIENTED_EDGE('',*,*,#5963,.F.);
#8547=ORIENTED_EDGE('',*,*,#5964,.F.);
#8548=ORIENTED_EDGE('',*,*,#5948,.F.);
#8549=ORIENTED_EDGE('',*,*,#5965,.F.);
#8550=ORIENTED_EDGE('',*,*,#5966,.T.);
#8551=ORIENTED_EDGE('',*,*,#5967,.T.);
#8552=ORIENTED_EDGE('',*,*,#5968,.T.);
#8553=ORIENTED_EDGE('',*,*,#5962,.F.);
#8554=ORIENTED_EDGE('',*,*,#5969,.F.);
#8555=ORIENTED_EDGE('',*,*,#5968,.F.);
#8556=ORIENTED_EDGE('',*,*,#5970,.F.);
#8557=ORIENTED_EDGE('',*,*,#5967,.F.);
#8558=ORIENTED_EDGE('',*,*,#5971,.F.);
#8559=ORIENTED_EDGE('',*,*,#5957,.F.);
#8560=ORIENTED_EDGE('',*,*,#5972,.F.);
#8561=ORIENTED_EDGE('',*,*,#5960,.F.);
#8562=ORIENTED_EDGE('',*,*,#5973,.F.);
#8563=ORIENTED_EDGE('',*,*,#5966,.F.);
#8564=ORIENTED_EDGE('',*,*,#5974,.F.);
#8565=ORIENTED_EDGE('',*,*,#5954,.F.);
#8566=ORIENTED_EDGE('',*,*,#5975,.F.);
#8567=ORIENTED_EDGE('',*,*,#5961,.F.);
#8568=ORIENTED_EDGE('',*,*,#5976,.F.);
#8569=ORIENTED_EDGE('',*,*,#5944,.F.);
#8570=ORIENTED_EDGE('',*,*,#5977,.F.);
#8571=ORIENTED_EDGE('',*,*,#5959,.F.);
#8572=ORIENTED_EDGE('',*,*,#5978,.F.);
#8573=ORIENTED_EDGE('',*,*,#5958,.F.);
#8574=ORIENTED_EDGE('',*,*,#5979,.F.);
#8575=ORIENTED_EDGE('',*,*,#5953,.F.);
#8576=ORIENTED_EDGE('',*,*,#5980,.F.);
#8577=ORIENTED_EDGE('',*,*,#5956,.F.);
#8578=ORIENTED_EDGE('',*,*,#5926,.F.);
#8579=ORIENTED_EDGE('',*,*,#5938,.F.);
#8580=ORIENTED_EDGE('',*,*,#5981,.F.);
#8581=ORIENTED_EDGE('',*,*,#5946,.F.);
#8582=ORIENTED_EDGE('',*,*,#5927,.F.);
#8583=ORIENTED_EDGE('',*,*,#5955,.F.);
#8584=ORIENTED_EDGE('',*,*,#5982,.F.);
#8585=ORIENTED_EDGE('',*,*,#5952,.F.);
#8586=ORIENTED_EDGE('',*,*,#5983,.F.);
#8587=ORIENTED_EDGE('',*,*,#5935,.F.);
#8588=ORIENTED_EDGE('',*,*,#5984,.F.);
#8589=ORIENTED_EDGE('',*,*,#5936,.F.);
#8590=ORIENTED_EDGE('',*,*,#5985,.F.);
#8591=ORIENTED_EDGE('',*,*,#5947,.F.);
#8592=ORIENTED_EDGE('',*,*,#5986,.F.);
#8593=ORIENTED_EDGE('',*,*,#5930,.F.);
#8594=ORIENTED_EDGE('',*,*,#5928,.F.);
#8595=ORIENTED_EDGE('',*,*,#5945,.F.);
#8596=ORIENTED_EDGE('',*,*,#5987,.F.);
#8597=ORIENTED_EDGE('',*,*,#5933,.F.);
#8598=ORIENTED_EDGE('',*,*,#5988,.F.);
#8599=ORIENTED_EDGE('',*,*,#5939,.F.);
#8600=ORIENTED_EDGE('',*,*,#5929,.F.);
#8601=ORIENTED_EDGE('',*,*,#5989,.F.);
#8602=ORIENTED_EDGE('',*,*,#5990,.F.);
#8603=ORIENTED_EDGE('',*,*,#5991,.F.);
#8604=ORIENTED_EDGE('',*,*,#5934,.F.);
#8605=ORIENTED_EDGE('',*,*,#5992,.F.);
#8606=ORIENTED_EDGE('',*,*,#5990,.T.);
#8607=ORIENTED_EDGE('',*,*,#5993,.F.);
#8608=ORIENTED_EDGE('',*,*,#5932,.F.);
#8609=ORIENTED_EDGE('',*,*,#5993,.T.);
#8610=ORIENTED_EDGE('',*,*,#5994,.F.);
#8611=ORIENTED_EDGE('',*,*,#5941,.T.);
#8612=ORIENTED_EDGE('',*,*,#5988,.T.);
#8613=ORIENTED_EDGE('',*,*,#5937,.T.);
#8614=ORIENTED_EDGE('',*,*,#5943,.T.);
#8615=ORIENTED_EDGE('',*,*,#5950,.T.);
#8616=ORIENTED_EDGE('',*,*,#5964,.T.);
#8617=ORIENTED_EDGE('',*,*,#5970,.T.);
#8618=ORIENTED_EDGE('',*,*,#5972,.T.);
#8619=ORIENTED_EDGE('',*,*,#5981,.T.);
#8620=ORIENTED_EDGE('',*,*,#5965,.T.);
#8621=ORIENTED_EDGE('',*,*,#5985,.T.);
#8622=ORIENTED_EDGE('',*,*,#5983,.T.);
#8623=ORIENTED_EDGE('',*,*,#5976,.T.);
#8624=ORIENTED_EDGE('',*,*,#5969,.T.);
#8625=ORIENTED_EDGE('',*,*,#5975,.T.);
#8626=ORIENTED_EDGE('',*,*,#5979,.T.);
#8627=ORIENTED_EDGE('',*,*,#5974,.T.);
#8628=ORIENTED_EDGE('',*,*,#5995,.T.);
#8629=ORIENTED_EDGE('',*,*,#5996,.T.);
#8630=ORIENTED_EDGE('',*,*,#5997,.T.);
#8631=ORIENTED_EDGE('',*,*,#5998,.T.);
#8632=ORIENTED_EDGE('',*,*,#5971,.T.);
#8633=ORIENTED_EDGE('',*,*,#5973,.T.);
#8634=ORIENTED_EDGE('',*,*,#5977,.T.);
#8635=ORIENTED_EDGE('',*,*,#5982,.T.);
#8636=ORIENTED_EDGE('',*,*,#5978,.T.);
#8637=ORIENTED_EDGE('',*,*,#5980,.T.);
#8638=ORIENTED_EDGE('',*,*,#5984,.T.);
#8639=ORIENTED_EDGE('',*,*,#5991,.T.);
#8640=ORIENTED_EDGE('',*,*,#5992,.T.);
#8641=ORIENTED_EDGE('',*,*,#5931,.T.);
#8642=ORIENTED_EDGE('',*,*,#5987,.T.);
#8643=ORIENTED_EDGE('',*,*,#5999,.F.);
#8644=ORIENTED_EDGE('',*,*,#5995,.F.);
#8645=ORIENTED_EDGE('',*,*,#6000,.F.);
#8646=ORIENTED_EDGE('',*,*,#5924,.F.);
#8647=ORIENTED_EDGE('',*,*,#6001,.F.);
#8648=ORIENTED_EDGE('',*,*,#6002,.F.);
#8649=ORIENTED_EDGE('',*,*,#6000,.T.);
#8650=ORIENTED_EDGE('',*,*,#5998,.F.);
#8651=ORIENTED_EDGE('',*,*,#6003,.F.);
#8652=ORIENTED_EDGE('',*,*,#6004,.F.);
#8653=ORIENTED_EDGE('',*,*,#6001,.T.);
#8654=ORIENTED_EDGE('',*,*,#5997,.F.);
#8655=ORIENTED_EDGE('',*,*,#5999,.T.);
#8656=ORIENTED_EDGE('',*,*,#5922,.F.);
#8657=ORIENTED_EDGE('',*,*,#6003,.T.);
#8658=ORIENTED_EDGE('',*,*,#5996,.F.);
#8659=ORIENTED_EDGE('',*,*,#5919,.T.);
#8660=ORIENTED_EDGE('',*,*,#5925,.F.);
#8661=ORIENTED_EDGE('',*,*,#6002,.T.);
#8662=ORIENTED_EDGE('',*,*,#6005,.T.);
#8663=ORIENTED_EDGE('',*,*,#5917,.T.);
#8664=ORIENTED_EDGE('',*,*,#6005,.F.);
#8665=ORIENTED_EDGE('',*,*,#6004,.T.);
#8666=ORIENTED_EDGE('',*,*,#5921,.T.);
#8667=ORIENTED_EDGE('',*,*,#5989,.T.);
#8668=ORIENTED_EDGE('',*,*,#5986,.T.);
#8669=ORIENTED_EDGE('',*,*,#5951,.T.);
#8670=ORIENTED_EDGE('',*,*,#5994,.T.);
#8994=PLANE('',#10841);
#8995=PLANE('',#10842);
#8996=PLANE('',#10904);
#8997=PLANE('',#10905);
#8998=PLANE('',#10906);
#8999=PLANE('',#10907);
#9000=PLANE('',#10910);
#9001=PLANE('',#10911);
#9002=PLANE('',#10922);
#9003=PLANE('',#10923);
#9534=ADVANCED_FACE('',(#2547),#594,.T.);
#9535=ADVANCED_FACE('',(#2548),#255,.T.);
#9536=ADVANCED_FACE('',(#2549),#595,.T.);
#9537=ADVANCED_FACE('',(#2550),#256,.T.);
#9538=ADVANCED_FACE('',(#2551),#596,.F.);
#9539=ADVANCED_FACE('',(#2552),#8994,.T.);
#9540=ADVANCED_FACE('',(#2553,#2023),#8995,.F.);
#9541=ADVANCED_FACE('',(#2554),#257,.T.);
#9542=ADVANCED_FACE('',(#2555),#195,.T.);
#9543=ADVANCED_FACE('',(#2556),#258,.T.);
#9544=ADVANCED_FACE('',(#2557),#597,.T.);
#9545=ADVANCED_FACE('',(#2558),#196,.T.);
#9546=ADVANCED_FACE('',(#2559),#197,.T.);
#9547=ADVANCED_FACE('',(#2560),#598,.T.);
#9548=ADVANCED_FACE('',(#2561),#198,.T.);
#9549=ADVANCED_FACE('',(#2562),#199,.T.);
#9550=ADVANCED_FACE('',(#2563),#200,.T.);
#9551=ADVANCED_FACE('',(#2564),#201,.T.);
#9552=ADVANCED_FACE('',(#2565),#599,.T.);
#9553=ADVANCED_FACE('',(#2566),#202,.T.);
#9554=ADVANCED_FACE('',(#2567),#600,.T.);
#9555=ADVANCED_FACE('',(#2568),#601,.T.);
#9556=ADVANCED_FACE('',(#2569),#602,.T.);
#9557=ADVANCED_FACE('',(#2570),#603,.T.);
#9558=ADVANCED_FACE('',(#2571),#604,.T.);
#9559=ADVANCED_FACE('',(#2572),#605,.T.);
#9560=ADVANCED_FACE('',(#2573),#606,.T.);
#9561=ADVANCED_FACE('',(#2574),#607,.T.);
#9562=ADVANCED_FACE('',(#2575),#608,.T.);
#9563=ADVANCED_FACE('',(#2576),#609,.T.);
#9564=ADVANCED_FACE('',(#2577),#610,.T.);
#9565=ADVANCED_FACE('',(#2578),#611,.F.);
#9566=ADVANCED_FACE('',(#2579),#612,.T.);
#9567=ADVANCED_FACE('',(#2580),#613,.T.);
#9568=ADVANCED_FACE('',(#2581),#8996,.F.);
#9569=ADVANCED_FACE('',(#2582),#8997,.T.);
#9570=ADVANCED_FACE('',(#2583),#8998,.F.);
#9571=ADVANCED_FACE('',(#2584,#2024),#8999,.F.);
#9572=ADVANCED_FACE('',(#2585),#9000,.F.);
#9573=ADVANCED_FACE('',(#2586),#9001,.F.);
#9574=ADVANCED_FACE('',(#2587),#614,.T.);
#9575=ADVANCED_FACE('',(#2588),#259,.T.);
#9576=ADVANCED_FACE('',(#2589),#615,.T.);
#9577=ADVANCED_FACE('',(#2590),#260,.T.);
#9578=ADVANCED_FACE('',(#2591),#616,.F.);
#9579=ADVANCED_FACE('',(#2592),#9002,.T.);
#9580=ADVANCED_FACE('',(#2593),#9003,.F.);
#9636=CLOSED_SHELL('',(#9534,#9535,#9536,#9537,#9538,#9539,#9540,#9541,
#9542,#9543,#9544,#9545,#9546,#9547,#9548,#9549,#9550,#9551,#9552,#9553,
#9554,#9555,#9556,#9557,#9558,#9559,#9560,#9561,#9562,#9563,#9564,#9565,
#9566,#9567,#9568,#9569,#9570,#9571,#9572,#9573,#9574,#9575,#9576,#9577,
#9578,#9579,#9580));
#10826=AXIS2_PLACEMENT_3D('',#17409,#13757,#13758);
#10827=AXIS2_PLACEMENT_3D('',#17410,#13759,#13760);
#10828=AXIS2_PLACEMENT_3D('',#17413,#13761,#13762);
#10829=AXIS2_PLACEMENT_3D('',#17417,#13764,#13765);
#10830=AXIS2_PLACEMENT_3D('',#17419,#13767,#13768);
#10831=AXIS2_PLACEMENT_3D('',#17422,#13769,#13770);
#10832=AXIS2_PLACEMENT_3D('',#17423,#13771,#13772);
#10833=AXIS2_PLACEMENT_3D('',#17424,#13773,#13774);
#10834=AXIS2_PLACEMENT_3D('',#17425,#13775,#13776);
#10835=AXIS2_PLACEMENT_3D('',#17428,#13777,#13778);
#10836=AXIS2_PLACEMENT_3D('',#17431,#13781,#13782);
#10837=AXIS2_PLACEMENT_3D('',#17432,#13783,#13784);
#10838=AXIS2_PLACEMENT_3D('',#17433,#13785,#13786);
#10839=AXIS2_PLACEMENT_3D('',#17434,#13787,#13788);
#10840=AXIS2_PLACEMENT_3D('',#17438,#13790,#13791);
#10841=AXIS2_PLACEMENT_3D('',#17440,#13793,#13794);
#10842=AXIS2_PLACEMENT_3D('',#17444,#13797,#13798);
#10843=AXIS2_PLACEMENT_3D('',#17453,#13803,#13804);
#10844=AXIS2_PLACEMENT_3D('',#17455,#13805,#13806);
#10845=AXIS2_PLACEMENT_3D('',#17457,#13807,#13808);
#10846=AXIS2_PLACEMENT_3D('',#17459,#13809,#13810);
#10847=AXIS2_PLACEMENT_3D('',#17460,#13811,#13812);
#10848=AXIS2_PLACEMENT_3D('',#17461,#13813,#13814);
#10849=AXIS2_PLACEMENT_3D('',#17464,#13815,#13816);
#10850=AXIS2_PLACEMENT_3D('',#17466,#13817,#13818);
#10851=AXIS2_PLACEMENT_3D('',#17467,#13819,#13820);
#10852=AXIS2_PLACEMENT_3D('',#17468,#13821,#13822);
#10853=AXIS2_PLACEMENT_3D('',#17471,#13823,#13824);
#10854=AXIS2_PLACEMENT_3D('',#17472,#13825,#13826);
#10855=AXIS2_PLACEMENT_3D('',#17474,#13827,#13828);
#10856=AXIS2_PLACEMENT_3D('',#17475,#13829,#13830);
#10857=AXIS2_PLACEMENT_3D('',#17476,#13831,#13832);
#10858=AXIS2_PLACEMENT_3D('',#17480,#13834,#13835);
#10859=AXIS2_PLACEMENT_3D('',#17482,#13837,#13838);
#10860=AXIS2_PLACEMENT_3D('',#17485,#13839,#13840);
#10861=AXIS2_PLACEMENT_3D('',#17486,#13841,#13842);
#10862=AXIS2_PLACEMENT_3D('',#17487,#13843,#13844);
#10863=AXIS2_PLACEMENT_3D('',#17488,#13845,#13846);
#10864=AXIS2_PLACEMENT_3D('',#17491,#13847,#13848);
#10865=AXIS2_PLACEMENT_3D('',#17493,#13849,#13850);
#10866=AXIS2_PLACEMENT_3D('',#17494,#13851,#13852);
#10867=AXIS2_PLACEMENT_3D('',#17495,#13853,#13854);
#10868=AXIS2_PLACEMENT_3D('',#17498,#13857,#13858);
#10869=AXIS2_PLACEMENT_3D('',#17501,#13859,#13860);
#10870=AXIS2_PLACEMENT_3D('',#17503,#13861,#13862);
#10871=AXIS2_PLACEMENT_3D('',#17504,#13863,#13864);
#10872=AXIS2_PLACEMENT_3D('',#17505,#13865,#13866);
#10873=AXIS2_PLACEMENT_3D('',#17507,#13867,#13868);
#10874=AXIS2_PLACEMENT_3D('',#17509,#13869,#13870);
#10875=AXIS2_PLACEMENT_3D('',#17510,#13871,#13872);
#10876=AXIS2_PLACEMENT_3D('',#17511,#13873,#13874);
#10877=AXIS2_PLACEMENT_3D('',#17514,#13875,#13876);
#10878=AXIS2_PLACEMENT_3D('',#17516,#13877,#13878);
#10879=AXIS2_PLACEMENT_3D('',#17517,#13879,#13880);
#10880=AXIS2_PLACEMENT_3D('',#17518,#13881,#13882);
#10881=AXIS2_PLACEMENT_3D('',#17521,#13883,#13884);
#10882=AXIS2_PLACEMENT_3D('',#17523,#13885,#13886);
#10883=AXIS2_PLACEMENT_3D('',#17524,#13887,#13888);
#10884=AXIS2_PLACEMENT_3D('',#17525,#13889,#13890);
#10885=AXIS2_PLACEMENT_3D('',#17528,#13893,#13894);
#10886=AXIS2_PLACEMENT_3D('',#17531,#13895,#13896);
#10887=AXIS2_PLACEMENT_3D('',#17533,#13897,#13898);
#10888=AXIS2_PLACEMENT_3D('',#17534,#13899,#13900);
#10889=AXIS2_PLACEMENT_3D('',#17535,#13901,#13902);
#10890=AXIS2_PLACEMENT_3D('',#17538,#13905,#13906);
#10891=AXIS2_PLACEMENT_3D('',#17541,#13909,#13910);
#10892=AXIS2_PLACEMENT_3D('',#17544,#13913,#13914);
#10893=AXIS2_PLACEMENT_3D('',#17547,#13917,#13918);
#10894=AXIS2_PLACEMENT_3D('',#17550,#13921,#13922);
#10895=AXIS2_PLACEMENT_3D('',#17553,#13925,#13926);
#10896=AXIS2_PLACEMENT_3D('',#17555,#13928,#13929);
#10897=AXIS2_PLACEMENT_3D('',#17557,#13931,#13932);
#10898=AXIS2_PLACEMENT_3D('',#17560,#13935,#13936);
#10899=AXIS2_PLACEMENT_3D('',#17563,#13939,#13940);
#10900=AXIS2_PLACEMENT_3D('',#17565,#13942,#13943);
#10901=AXIS2_PLACEMENT_3D('',#17567,#13945,#13946);
#10902=AXIS2_PLACEMENT_3D('',#17571,#13948,#13949);
#10903=AXIS2_PLACEMENT_3D('',#17573,#13951,#13952);
#10904=AXIS2_PLACEMENT_3D('',#17576,#13955,#13956);
#10905=AXIS2_PLACEMENT_3D('',#17578,#13958,#13959);
#10906=AXIS2_PLACEMENT_3D('',#17579,#13960,#13961);
#10907=AXIS2_PLACEMENT_3D('',#17580,#13962,#13963);
#10908=AXIS2_PLACEMENT_3D('',#17585,#13965,#13966);
#10909=AXIS2_PLACEMENT_3D('',#17588,#13968,#13969);
#10910=AXIS2_PLACEMENT_3D('',#17589,#13970,#13971);
#10911=AXIS2_PLACEMENT_3D('',#17590,#13972,#13973);
#10912=AXIS2_PLACEMENT_3D('',#17591,#13974,#13975);
#10913=AXIS2_PLACEMENT_3D('',#17592,#13976,#13977);
#10914=AXIS2_PLACEMENT_3D('',#17593,#13978,#13979);
#10915=AXIS2_PLACEMENT_3D('',#17594,#13980,#13981);
#10916=AXIS2_PLACEMENT_3D('',#17596,#13982,#13983);
#10917=AXIS2_PLACEMENT_3D('',#17597,#13984,#13985);
#10918=AXIS2_PLACEMENT_3D('',#17598,#13986,#13987);
#10919=AXIS2_PLACEMENT_3D('',#17599,#13988,#13989);
#10920=AXIS2_PLACEMENT_3D('',#17601,#13991,#13992);
#10921=AXIS2_PLACEMENT_3D('',#17602,#13993,#13994);
#10922=AXIS2_PLACEMENT_3D('',#17604,#13996,#13997);
#10923=AXIS2_PLACEMENT_3D('',#17605,#13998,#13999);
#13757=DIRECTION('axis',(0.,0.,1.));
#13758=DIRECTION('refdir',(1.,0.,0.));
#13759=DIRECTION('center_axis',(1.,0.,0.));
#13760=DIRECTION('ref_axis',(0.,0.707106781186519,-0.707106781186576));
#13761=DIRECTION('center_axis',(1.,0.,0.));
#13762=DIRECTION('ref_axis',(0.,0.,-1.));
#13763=DIRECTION('',(1.,0.,0.));
#13764=DIRECTION('center_axis',(-1.,0.,0.));
#13765=DIRECTION('ref_axis',(0.,1.,0.));
#13766=DIRECTION('',(-1.,0.,0.));
#13767=DIRECTION('center_axis',(0.,0.,1.));
#13768=DIRECTION('ref_axis',(-1.,0.,0.));
#13769=DIRECTION('center_axis',(1.,0.,0.));
#13770=DIRECTION('ref_axis',(0.,-1.,0.));
#13771=DIRECTION('center_axis',(0.,0.,-1.));
#13772=DIRECTION('ref_axis',(-1.,0.,0.));
#13773=DIRECTION('center_axis',(0.,0.,1.));
#13774=DIRECTION('ref_axis',(-1.,0.,0.));
#13775=DIRECTION('center_axis',(-1.,0.,0.));
#13776=DIRECTION('ref_axis',(0.,-0.707106781186561,-0.707106781186534));
#13777=DIRECTION('center_axis',(1.,0.,0.));
#13778=DIRECTION('ref_axis',(0.,-1.,0.));
#13779=DIRECTION('',(1.,0.,0.));
#13780=DIRECTION('',(-1.,0.,0.));
#13781=DIRECTION('center_axis',(0.,0.,1.));
#13782=DIRECTION('ref_axis',(1.,0.,0.));
#13783=DIRECTION('center_axis',(0.,0.,-1.));
#13784=DIRECTION('ref_axis',(1.,0.,0.));
#13785=DIRECTION('center_axis',(0.,0.,1.));
#13786=DIRECTION('ref_axis',(1.,0.,0.));
#13787=DIRECTION('center_axis',(0.,0.,1.));
#13788=DIRECTION('ref_axis',(0.,-1.,0.));
#13789=DIRECTION('',(0.,0.,-1.));
#13790=DIRECTION('center_axis',(0.,0.,1.));
#13791=DIRECTION('ref_axis',(-1.,0.,0.));
#13792=DIRECTION('',(0.,0.,-1.));
#13793=DIRECTION('center_axis',(0.,1.,0.));
#13794=DIRECTION('ref_axis',(1.,0.,0.));
#13795=DIRECTION('',(1.,0.,0.));
#13796=DIRECTION('',(0.,0.,-1.));
#13797=DIRECTION('center_axis',(0.,0.,1.));
#13798=DIRECTION('ref_axis',(1.,0.,0.));
#13799=DIRECTION('',(-1.,0.,0.));
#13800=DIRECTION('',(0.,1.,0.));
#13801=DIRECTION('',(1.,0.,0.));
#13802=DIRECTION('',(0.,-1.,0.));
#13803=DIRECTION('center_axis',(0.,-1.,0.));
#13804=DIRECTION('ref_axis',(0.,0.,-1.));
#13805=DIRECTION('center_axis',(1.,0.,0.));
#13806=DIRECTION('ref_axis',(0.,0.,-1.));
#13807=DIRECTION('center_axis',(0.,-1.,0.));
#13808=DIRECTION('ref_axis',(0.70710678118654,0.,0.707106781186555));
#13809=DIRECTION('center_axis',(0.,0.,1.));
#13810=DIRECTION('ref_axis',(0.,1.,0.));
#13811=DIRECTION('center_axis',(0.,1.,0.));
#13812=DIRECTION('ref_axis',(1.,0.,0.));
#13813=DIRECTION('center_axis',(0.816496580927734,-0.408248290463867,0.408248290463843));
#13814=DIRECTION('ref_axis',(0.577350269189598,0.577350269189645,-0.577350269189634));
#13815=DIRECTION('center_axis',(-1.,0.,0.));
#13816=DIRECTION('ref_axis',(0.,0.,-1.));
#13817=DIRECTION('center_axis',(-9.25185853854317E-16,0.,1.));
#13818=DIRECTION('ref_axis',(0.,1.,0.));
#13819=DIRECTION('center_axis',(0.,-1.,0.));
#13820=DIRECTION('ref_axis',(1.,0.,0.));
#13821=DIRECTION('center_axis',(0.,-1.,0.));
#13822=DIRECTION('ref_axis',(0.,0.,-1.));
#13823=DIRECTION('center_axis',(0.,1.,0.));
#13824=DIRECTION('ref_axis',(0.70710678118654,0.,0.707106781186555));
#13825=DIRECTION('center_axis',(1.,0.,0.));
#13826=DIRECTION('ref_axis',(0.,-1.,0.));
#13827=DIRECTION('center_axis',(-5.92118946466763E-14,-1.,0.));
#13828=DIRECTION('ref_axis',(0.,0.,1.));
#13829=DIRECTION('center_axis',(0.,0.,1.));
#13830=DIRECTION('ref_axis',(-1.,0.,0.));
#13831=DIRECTION('center_axis',(0.,0.,1.));
#13832=DIRECTION('ref_axis',(-0.707106781186547,-0.707106781186547,0.));
#13833=DIRECTION('',(0.,0.,1.));
#13834=DIRECTION('center_axis',(0.707106781186576,0.,-0.707106781186519));
#13835=DIRECTION('ref_axis',(0.707106781186519,0.,0.707106781186576));
#13836=DIRECTION('',(0.,0.,-1.));
#13837=DIRECTION('center_axis',(0.827465426020362,0.538877990790925,-0.157833709270471));
#13838=DIRECTION('ref_axis',(-0.561516668266355,0.794104487760816,-0.232587819494453));
#13839=DIRECTION('center_axis',(0.707106781186544,3.663549070262E-14,0.707106781186551));
#13840=DIRECTION('ref_axis',(-0.707106781186551,0.,0.707106781186544));
#13841=DIRECTION('center_axis',(1.,0.,2.96059473233375E-14));
#13842=DIRECTION('ref_axis',(0.,1.,0.));
#13843=DIRECTION('center_axis',(0.,-1.,0.));
#13844=DIRECTION('ref_axis',(0.,0.,-1.));
#13845=DIRECTION('center_axis',(-0.408248290463871,0.408248290463824,-0.816496580927742));
#13846=DIRECTION('ref_axis',(0.577350269189681,-0.577350269189586,-0.57735026918961));
#13847=DIRECTION('center_axis',(0.,1.,0.));
#13848=DIRECTION('ref_axis',(0.,0.,-1.));
#13849=DIRECTION('center_axis',(0.,9.25185853854317E-16,1.));
#13850=DIRECTION('ref_axis',(1.,0.,0.));
#13851=DIRECTION('center_axis',(-1.,0.,-5.9211894646675E-14));
#13852=DIRECTION('ref_axis',(0.,-1.,0.));
#13853=DIRECTION('center_axis',(-1.,0.,0.));
#13854=DIRECTION('ref_axis',(0.,-0.707106781186519,-0.707106781186576));
#13855=DIRECTION('',(1.,0.,0.));
#13856=DIRECTION('',(-1.,0.,0.));
#13857=DIRECTION('center_axis',(0.408248290463863,0.408248290463816,-0.81649658092775));
#13858=DIRECTION('ref_axis',(0.577350269189665,0.577350269189618,0.577350269189594));
#13859=DIRECTION('center_axis',(0.,0.,-1.));
#13860=DIRECTION('ref_axis',(1.,0.,0.));
#13861=DIRECTION('center_axis',(-1.,0.,-5.9211894646675E-14));
#13862=DIRECTION('ref_axis',(0.,1.,0.));
#13863=DIRECTION('center_axis',(0.,-1.,0.));
#13864=DIRECTION('ref_axis',(0.,0.,1.));
#13865=DIRECTION('center_axis',(0.827465426020388,-0.538877990790895,-0.157833709270442));
#13866=DIRECTION('ref_axis',(-0.561516668266318,-0.794104487760845,-0.232587819494444));
#13867=DIRECTION('center_axis',(0.,1.,0.));
#13868=DIRECTION('ref_axis',(-0.707106781186544,0.,0.707106781186551));
#13869=DIRECTION('center_axis',(1.,-2.96059473233364E-14,0.));
#13870=DIRECTION('ref_axis',(0.,0.,-1.));
#13871=DIRECTION('center_axis',(0.70710678118657,0.,0.707106781186525));
#13872=DIRECTION('ref_axis',(0.,-1.,0.));
#13873=DIRECTION('center_axis',(-0.182143211721525,-0.8794652240646,0.439732612032324));
#13874=DIRECTION('ref_axis',(-0.336556770590774,0.475963149478001,0.812519920068728));
#13875=DIRECTION('center_axis',(1.,0.,0.));
#13876=DIRECTION('ref_axis',(0.,0.,1.));
#13877=DIRECTION('center_axis',(-0.70710678118654,0.,-0.707106781186555));
#13878=DIRECTION('ref_axis',(0.,1.,0.));
#13879=DIRECTION('center_axis',(0.,-1.,0.));
#13880=DIRECTION('ref_axis',(-0.707106781186551,0.,0.707106781186544));
#13881=DIRECTION('center_axis',(0.408248290463908,-0.408248290463861,-0.816496580927704));
#13882=DIRECTION('ref_axis',(0.577350269189642,-0.577350269189594,0.577350269189642));
#13883=DIRECTION('center_axis',(0.,1.,-5.9211894646675E-14));
#13884=DIRECTION('ref_axis',(1.,0.,0.));
#13885=DIRECTION('center_axis',(-1.,0.,0.));
#13886=DIRECTION('ref_axis',(0.,0.,1.));
#13887=DIRECTION('center_axis',(0.,0.,-1.));
#13888=DIRECTION('ref_axis',(0.,-1.,0.));
#13889=DIRECTION('center_axis',(0.,0.,-1.));
#13890=DIRECTION('ref_axis',(0.707106781186589,-0.707106781186506,0.));
#13891=DIRECTION('',(0.,0.,1.));
#13892=DIRECTION('',(0.,0.,-1.));
#13893=DIRECTION('center_axis',(0.182143211721517,-0.879465224064606,-0.439732612032315));
#13894=DIRECTION('ref_axis',(-0.336556770590767,-0.475963149477992,0.812519920068736));
#13895=DIRECTION('center_axis',(0.,1.,0.));
#13896=DIRECTION('ref_axis',(0.,0.,1.));
#13897=DIRECTION('center_axis',(-0.70710678118654,0.,-0.707106781186555));
#13898=DIRECTION('ref_axis',(-0.707106781186555,0.,0.70710678118654));
#13899=DIRECTION('center_axis',(1.,0.,0.));
#13900=DIRECTION('ref_axis',(0.,-1.,0.));
#13901=DIRECTION('center_axis',(-1.,0.,0.));
#13902=DIRECTION('ref_axis',(0.,-0.707106781186558,0.707106781186537));
#13903=DIRECTION('',(1.,0.,0.));
#13904=DIRECTION('',(-1.,0.,0.));
#13905=DIRECTION('center_axis',(-0.707106781186547,0.,-0.707106781186548));
#13906=DIRECTION('ref_axis',(-0.499999999999997,-0.707106781186559,0.499999999999986));
#13907=DIRECTION('',(0.707106781186547,0.,0.707106781186548));
#13908=DIRECTION('',(-0.707106781186547,0.,-0.707106781186548));
#13909=DIRECTION('center_axis',(0.,-1.,0.));
#13910=DIRECTION('ref_axis',(-0.382683432365094,0.,0.923879532511285));
#13911=DIRECTION('',(0.,1.,0.));
#13912=DIRECTION('',(0.,-1.,0.));
#13913=DIRECTION('center_axis',(0.,-1.,0.));
#13914=DIRECTION('ref_axis',(0.707106781186558,0.,0.707106781186537));
#13915=DIRECTION('',(0.,1.,0.));
#13916=DIRECTION('',(0.,-1.,0.));
#13917=DIRECTION('center_axis',(0.707106781186547,0.,0.707106781186548));
#13918=DIRECTION('ref_axis',(-0.499999999999997,0.707106781186559,0.499999999999986));
#13919=DIRECTION('',(-0.707106781186547,0.,-0.707106781186548));
#13920=DIRECTION('',(0.707106781186547,0.,0.707106781186548));
#13921=DIRECTION('center_axis',(1.,0.,0.));
#13922=DIRECTION('ref_axis',(0.,0.707106781186558,0.707106781186537));
#13923=DIRECTION('',(-1.,0.,0.));
#13924=DIRECTION('',(1.,0.,0.));
#13925=DIRECTION('center_axis',(1.,0.,0.));
#13926=DIRECTION('ref_axis',(0.,-0.707106781186561,-0.707106781186534));
#13927=DIRECTION('',(1.,0.,0.));
#13928=DIRECTION('center_axis',(0.,-1.,0.));
#13929=DIRECTION('ref_axis',(-0.923879532511297,0.,-0.382683432365066));
#13930=DIRECTION('',(0.,-1.,0.));
#13931=DIRECTION('center_axis',(0.,0.,-1.));
#13932=DIRECTION('ref_axis',(0.707106781186506,0.707106781186589,0.));
#13933=DIRECTION('',(0.,0.,1.));
#13934=DIRECTION('',(0.,0.,-1.));
#13935=DIRECTION('center_axis',(0.,-1.,0.));
#13936=DIRECTION('ref_axis',(0.707106781186519,0.,-0.707106781186576));
#13937=DIRECTION('',(0.,1.,0.));
#13938=DIRECTION('',(0.,-1.,0.));
#13939=DIRECTION('center_axis',(-1.,0.,0.));
#13940=DIRECTION('ref_axis',(0.,0.707106781186561,-0.707106781186534));
#13941=DIRECTION('',(-1.,0.,0.));
#13942=DIRECTION('center_axis',(0.,-1.,0.));
#13943=DIRECTION('ref_axis',(0.707106781186519,0.,0.707106781186576));
#13944=DIRECTION('',(0.,1.,0.));
#13945=DIRECTION('center_axis',(-1.,0.,0.));
#13946=DIRECTION('ref_axis',(0.,0.707106781186561,-0.707106781186534));
#13947=DIRECTION('',(1.,0.,0.));
#13948=DIRECTION('center_axis',(-0.707106781186555,0.,0.70710678118654));
#13949=DIRECTION('ref_axis',(-0.70710678118654,0.,-0.707106781186555));
#13950=DIRECTION('',(-1.,0.,0.));
#13951=DIRECTION('center_axis',(0.,0.,1.));
#13952=DIRECTION('ref_axis',(-0.707106781186506,0.707106781186589,0.));
#13953=DIRECTION('',(0.,0.,1.));
#13954=DIRECTION('',(0.,0.,-1.));
#13955=DIRECTION('center_axis',(1.,0.,0.));
#13956=DIRECTION('ref_axis',(0.,0.,-1.));
#13957=DIRECTION('',(0.,1.,0.));
#13958=DIRECTION('center_axis',(0.,-1.,0.));
#13959=DIRECTION('ref_axis',(-1.,0.,0.));
#13960=DIRECTION('center_axis',(-1.,0.,0.));
#13961=DIRECTION('ref_axis',(0.,0.,1.));
#13962=DIRECTION('center_axis',(0.,0.,-1.));
#13963=DIRECTION('ref_axis',(-1.,0.,0.));
#13964=DIRECTION('',(-1.,0.,0.));
#13965=DIRECTION('center_axis',(0.,0.,-1.));
#13966=DIRECTION('ref_axis',(-1.,0.,0.));
#13967=DIRECTION('',(1.,0.,0.));
#13968=DIRECTION('center_axis',(0.,0.,-1.));
#13969=DIRECTION('ref_axis',(1.,0.,0.));
#13970=DIRECTION('center_axis',(0.707106781186548,0.,-0.707106781186547));
#13971=DIRECTION('ref_axis',(-0.707106781186547,0.,-0.707106781186548));
#13972=DIRECTION('center_axis',(0.,-1.,0.));
#13973=DIRECTION('ref_axis',(0.,0.,1.));
#13974=DIRECTION('center_axis',(-1.,0.,0.));
#13975=DIRECTION('ref_axis',(0.,0.707106781186516,0.707106781186579));
#13976=DIRECTION('center_axis',(-1.,0.,0.));
#13977=DIRECTION('ref_axis',(0.,0.,1.));
#13978=DIRECTION('center_axis',(1.,0.,0.));
#13979=DIRECTION('ref_axis',(0.,1.,0.));
#13980=DIRECTION('center_axis',(0.,0.,-1.));
#13981=DIRECTION('ref_axis',(1.,0.,0.));
#13982=DIRECTION('center_axis',(-1.,0.,0.));
#13983=DIRECTION('ref_axis',(0.,-1.,0.));
#13984=DIRECTION('center_axis',(0.,0.,1.));
#13985=DIRECTION('ref_axis',(1.,0.,0.));
#13986=DIRECTION('center_axis',(1.,0.,0.));
#13987=DIRECTION('ref_axis',(0.,-0.707106781186558,0.707106781186537));
#13988=DIRECTION('center_axis',(-1.,0.,0.));
#13989=DIRECTION('ref_axis',(0.,-1.,0.));
#13990=DIRECTION('',(-1.,0.,0.));
#13991=DIRECTION('center_axis',(0.,0.,-1.));
#13992=DIRECTION('ref_axis',(-1.,0.,0.));
#13993=DIRECTION('center_axis',(0.,0.,1.));
#13994=DIRECTION('ref_axis',(0.,1.,0.));
#13995=DIRECTION('',(0.,0.,-1.));
#13996=DIRECTION('center_axis',(0.,-1.,0.));
#13997=DIRECTION('ref_axis',(-1.,0.,0.));
#13998=DIRECTION('center_axis',(0.,0.,1.));
#13999=DIRECTION('ref_axis',(1.,0.,0.));
#17409=CARTESIAN_POINT('',(0.,0.,0.));
#17410=CARTESIAN_POINT('Origin',(69.9040264336917,-84.8,3.08953555269655));
#17411=CARTESIAN_POINT('',(104.475451921837,-84.8,2.78953555269655));
#17412=CARTESIAN_POINT('',(104.475451921837,-84.5,3.08953555269655));
#17413=CARTESIAN_POINT('Origin',(104.475451921837,-84.8,3.08953555269655));
#17414=CARTESIAN_POINT('',(77.8080528673835,-84.8,2.78953555269655));
#17415=CARTESIAN_POINT('',(69.9040264336917,-84.8,2.78953555269655));
#17416=CARTESIAN_POINT('',(77.8080528673835,-84.5,3.08953555269655));
#17417=CARTESIAN_POINT('Origin',(77.8080528673835,-84.8,3.08953555269655));
#17418=CARTESIAN_POINT('',(69.9040264336917,-84.5,3.08953555269655));
#17419=CARTESIAN_POINT('Origin',(77.8080528673835,-80.,3.08953555269655));
#17420=CARTESIAN_POINT('',(77.8080528673835,-75.5,3.08953555269655));
#17421=CARTESIAN_POINT('',(77.8080528673835,-75.2,2.78953555269655));
#17422=CARTESIAN_POINT('Origin',(77.8080528673835,-75.2,3.08953555269655));
#17423=CARTESIAN_POINT('Origin',(77.8080528673835,-80.,3.08953555269655));
#17424=CARTESIAN_POINT('Origin',(77.8080528673835,-80.,2.78953555269655));
#17425=CARTESIAN_POINT('Origin',(83.2377259609183,-75.2,3.08953555269655));
#17426=CARTESIAN_POINT('',(104.475451921837,-75.5,3.08953555269655));
#17427=CARTESIAN_POINT('',(104.475451921837,-75.2,2.78953555269655));
#17428=CARTESIAN_POINT('Origin',(104.475451921837,-75.2,3.08953555269655));
#17429=CARTESIAN_POINT('',(83.2377259609183,-75.5,3.08953555269655));
#17430=CARTESIAN_POINT('',(83.2377259609183,-75.2,2.78953555269655));
#17431=CARTESIAN_POINT('Origin',(104.475451921837,-80.,3.08953555269655));
#17432=CARTESIAN_POINT('Origin',(104.475451921837,-80.,3.08953555269655));
#17433=CARTESIAN_POINT('Origin',(104.475451921837,-80.,2.78953555269655));
#17434=CARTESIAN_POINT('Origin',(77.8080528673835,-80.,10.7895355526966));
#17435=CARTESIAN_POINT('',(77.8080528673835,-75.5,10.4895355526966));
#17436=CARTESIAN_POINT('',(77.8080528673835,-75.5,10.7895355526966));
#17437=CARTESIAN_POINT('',(77.8080528673835,-84.5,10.4895355526966));
#17438=CARTESIAN_POINT('Origin',(77.8080528673835,-80.,10.4895355526966));
#17439=CARTESIAN_POINT('',(77.8080528673835,-84.5,10.7895355526966));
#17440=CARTESIAN_POINT('Origin',(77.8080528673835,-84.5,10.7895355526966));
#17441=CARTESIAN_POINT('',(104.475451921837,-84.5,10.4895355526966));
#17442=CARTESIAN_POINT('',(94.9040264336917,-84.5,10.4895355526966));
#17443=CARTESIAN_POINT('',(104.475451921837,-84.5,10.7895355526966));
#17444=CARTESIAN_POINT('Origin',(62.,-90.,2.78953555269655));
#17445=CARTESIAN_POINT('',(109.7,-89.7,2.78953555269655));
#17446=CARTESIAN_POINT('',(62.7242640687119,-89.7,2.78953555269655));
#17447=CARTESIAN_POINT('',(74.5,-89.7,2.78953555269655));
#17448=CARTESIAN_POINT('',(62.7242640687119,-70.3,2.78953555269655));
#17449=CARTESIAN_POINT('',(62.7242640687119,-90.,2.78953555269655));
#17450=CARTESIAN_POINT('',(109.7,-70.3,2.78953555269655));
#17451=CARTESIAN_POINT('',(74.5,-70.3,2.78953555269655));
#17452=CARTESIAN_POINT('',(109.7,-90.,2.78953555269655));
#17453=CARTESIAN_POINT('Origin',(109.7,-70.3,2.48953555269655));
#17454=CARTESIAN_POINT('',(109.7,-70.,3.08953555269655));
#17455=CARTESIAN_POINT('Origin',(109.7,-70.3,3.08953555269655));
#17456=CARTESIAN_POINT('',(110.3,-70.,2.48953555269655));
#17457=CARTESIAN_POINT('Origin',(109.7,-70.,2.48953555269655));
#17458=CARTESIAN_POINT('',(110.,-70.3,2.48953555269655));
#17459=CARTESIAN_POINT('Origin',(110.3,-70.3,2.48953555269655));
#17460=CARTESIAN_POINT('Origin',(109.7,-70.3,2.48953555269655));
#17461=CARTESIAN_POINT('Origin',(111.7,-70.3,0.3));
#17462=CARTESIAN_POINT('',(111.7,-70.3,0.));
#17463=CARTESIAN_POINT('',(111.7,-70.,0.3));
#17464=CARTESIAN_POINT('Origin',(111.7,-70.3,0.3));
#17465=CARTESIAN_POINT('',(112.,-70.3,0.3));
#17466=CARTESIAN_POINT('Origin',(111.7,-70.3,0.3));
#17467=CARTESIAN_POINT('Origin',(111.7,-70.3,0.3));
#17468=CARTESIAN_POINT('Origin',(109.7,-89.7,2.48953555269655));
#17469=CARTESIAN_POINT('',(109.7,-90.,3.08953555269655));
#17470=CARTESIAN_POINT('',(110.3,-90.,2.48953555269655));
#17471=CARTESIAN_POINT('Origin',(109.7,-90.,2.48953555269655));
#17472=CARTESIAN_POINT('Origin',(109.7,-89.7,3.08953555269655));
#17473=CARTESIAN_POINT('',(110.,-89.7,2.48953555269655));
#17474=CARTESIAN_POINT('Origin',(109.7,-89.7,2.48953555269655));
#17475=CARTESIAN_POINT('Origin',(110.3,-89.7,2.48953555269655));
#17476=CARTESIAN_POINT('Origin',(110.3,-89.7,4.09215166452241));
#17477=CARTESIAN_POINT('',(110.,-89.7,0.));
#17478=CARTESIAN_POINT('',(110.,-89.7,4.09215166452241));
#17479=CARTESIAN_POINT('',(110.3,-90.,0.3));
#17480=CARTESIAN_POINT('Origin',(110.3,-89.7,0.3));
#17481=CARTESIAN_POINT('',(110.3,-90.,4.09215166452241));
#17482=CARTESIAN_POINT('Origin',(62.7242640687119,-70.3,3.08953555269655));
#17483=CARTESIAN_POINT('',(62.512132034356,-70.3,3.30166758705252));
#17484=CARTESIAN_POINT('',(62.7242640687119,-70.,3.08953555269655));
#17485=CARTESIAN_POINT('Origin',(62.7242640687119,-70.3,3.08953555269656));
#17486=CARTESIAN_POINT('Origin',(62.7242640687119,-70.3,3.08953555269655));
#17487=CARTESIAN_POINT('Origin',(62.7242640687119,-70.3,3.08953555269655));
#17488=CARTESIAN_POINT('Origin',(111.7,-89.7,0.3));
#17489=CARTESIAN_POINT('',(111.7,-89.7,0.));
#17490=CARTESIAN_POINT('',(112.,-89.7,0.3));
#17491=CARTESIAN_POINT('Origin',(111.7,-89.7,0.3));
#17492=CARTESIAN_POINT('',(111.7,-90.,0.3));
#17493=CARTESIAN_POINT('Origin',(111.7,-89.7,0.3));
#17494=CARTESIAN_POINT('Origin',(111.7,-89.7,0.3));
#17495=CARTESIAN_POINT('Origin',(98.5,-89.7,0.3));
#17496=CARTESIAN_POINT('',(98.5,-90.,0.3));
#17497=CARTESIAN_POINT('',(98.5,-89.7,0.));
#17498=CARTESIAN_POINT('Origin',(111.7,-70.3,10.4895355526966));
#17499=CARTESIAN_POINT('',(112.,-70.3,10.4895355526966));
#17500=CARTESIAN_POINT('',(111.7,-70.,10.4895355526966));
#17501=CARTESIAN_POINT('Origin',(111.7,-70.3,10.4895355526966));
#17502=CARTESIAN_POINT('',(111.7,-70.3,10.7895355526966));
#17503=CARTESIAN_POINT('Origin',(111.7,-70.3,10.4895355526966));
#17504=CARTESIAN_POINT('Origin',(111.7,-70.3,10.4895355526966));
#17505=CARTESIAN_POINT('Origin',(62.7242640687119,-89.7,3.08953555269655));
#17506=CARTESIAN_POINT('',(62.512132034356,-89.7,3.30166758705252));
#17507=CARTESIAN_POINT('Origin',(62.7242640687119,-89.7,3.08953555269655));
#17508=CARTESIAN_POINT('',(62.7242640687119,-90.,3.08953555269655));
#17509=CARTESIAN_POINT('Origin',(62.7242640687119,-89.7,3.08953555269655));
#17510=CARTESIAN_POINT('Origin',(62.7242640687119,-89.7,3.08953555269655));
#17511=CARTESIAN_POINT('Origin',(70.1242640687119,-70.3,10.4895355526966));
#17512=CARTESIAN_POINT('',(70.1242640687119,-70.3,10.7895355526966));
#17513=CARTESIAN_POINT('',(70.1242640687119,-70.,10.4895355526966));
#17514=CARTESIAN_POINT('Origin',(70.1242640687119,-70.3,10.4895355526966));
#17515=CARTESIAN_POINT('',(69.9121320343559,-70.3,10.7016675870525));
#17516=CARTESIAN_POINT('Origin',(70.1242640687119,-70.3,10.4895355526966));
#17517=CARTESIAN_POINT('Origin',(70.1242640687119,-70.3,10.4895355526966));
#17518=CARTESIAN_POINT('Origin',(111.7,-89.7,10.4895355526966));
#17519=CARTESIAN_POINT('',(112.,-89.7,10.4895355526966));
#17520=CARTESIAN_POINT('',(111.7,-89.7,10.7895355526966));
#17521=CARTESIAN_POINT('Origin',(111.7,-89.7,10.4895355526966));
#17522=CARTESIAN_POINT('',(111.7,-90.,10.4895355526966));
#17523=CARTESIAN_POINT('Origin',(111.7,-89.7,10.4895355526966));
#17524=CARTESIAN_POINT('Origin',(111.7,-89.7,10.4895355526966));
#17525=CARTESIAN_POINT('Origin',(111.7,-89.7,2.69738388817414));
#17526=CARTESIAN_POINT('',(111.7,-90.,2.69738388817414));
#17527=CARTESIAN_POINT('',(112.,-89.7,2.69738388817414));
#17528=CARTESIAN_POINT('Origin',(70.1242640687119,-89.7,10.4895355526966));
#17529=CARTESIAN_POINT('',(70.1242640687119,-89.7,10.7895355526966));
#17530=CARTESIAN_POINT('',(69.9121320343559,-89.7,10.7016675870525));
#17531=CARTESIAN_POINT('Origin',(70.1242640687119,-89.7,10.4895355526966));
#17532=CARTESIAN_POINT('',(70.1242640687119,-90.,10.4895355526966));
#17533=CARTESIAN_POINT('Origin',(70.1242640687119,-89.7,10.4895355526966));
#17534=CARTESIAN_POINT('Origin',(70.1242640687119,-89.7,10.4895355526966));
#17535=CARTESIAN_POINT('Origin',(99.5,-89.7,10.4895355526966));
#17536=CARTESIAN_POINT('',(99.5,-89.7,10.7895355526966));
#17537=CARTESIAN_POINT('',(99.5,-90.,10.4895355526966));
#17538=CARTESIAN_POINT('Origin',(73.1134400902689,-89.7,13.4787115742535));
#17539=CARTESIAN_POINT('',(72.9013080559129,-89.7,13.6908436086095));
#17540=CARTESIAN_POINT('',(73.1134400902689,-90.,13.4787115742535));
#17541=CARTESIAN_POINT('Origin',(70.1242640687119,-90.,10.4895355526966));
#17542=CARTESIAN_POINT('',(69.9121320343559,-90.,10.7016675870525));
#17543=CARTESIAN_POINT('',(70.1242640687119,-90.,10.7895355526966));
#17544=CARTESIAN_POINT('Origin',(111.7,-90.,10.4895355526966));
#17545=CARTESIAN_POINT('',(111.7,-90.,10.7895355526966));
#17546=CARTESIAN_POINT('',(112.,-90.,10.4895355526966));
#17547=CARTESIAN_POINT('Origin',(73.1134400902689,-70.3,13.4787115742535));
#17548=CARTESIAN_POINT('',(72.9013080559129,-70.3,13.6908436086095));
#17549=CARTESIAN_POINT('',(73.1134400902689,-70.,13.4787115742535));
#17550=CARTESIAN_POINT('Origin',(99.5,-70.3,10.4895355526966));
#17551=CARTESIAN_POINT('',(99.5,-70.3,10.7895355526966));
#17552=CARTESIAN_POINT('',(99.5,-70.,10.4895355526966));
#17553=CARTESIAN_POINT('Origin',(74.5,-89.7,3.08953555269655));
#17554=CARTESIAN_POINT('',(74.5,-90.,3.08953555269655));
#17555=CARTESIAN_POINT('Origin',(62.7242640687119,-90.,3.08953555269655));
#17556=CARTESIAN_POINT('',(62.512132034356,-90.,3.30166758705252));
#17557=CARTESIAN_POINT('Origin',(111.7,-70.3,2.69738388817414));
#17558=CARTESIAN_POINT('',(112.,-70.3,2.69738388817414));
#17559=CARTESIAN_POINT('',(111.7,-70.,2.69738388817414));
#17560=CARTESIAN_POINT('Origin',(111.7,-90.,0.3));
#17561=CARTESIAN_POINT('',(112.,-90.,0.3));
#17562=CARTESIAN_POINT('',(111.7,-90.,0.));
#17563=CARTESIAN_POINT('Origin',(74.5,-70.3,3.08953555269655));
#17564=CARTESIAN_POINT('',(74.5,-70.,3.08953555269655));
#17565=CARTESIAN_POINT('Origin',(109.7,-90.,2.48953555269655));
#17566=CARTESIAN_POINT('',(110.,-90.,2.48953555269655));
#17567=CARTESIAN_POINT('Origin',(98.5,-70.3,0.3));
#17568=CARTESIAN_POINT('',(110.,-70.3,0.));
#17569=CARTESIAN_POINT('',(98.5,-70.3,0.));
#17570=CARTESIAN_POINT('',(110.3,-70.,0.3));
#17571=CARTESIAN_POINT('Origin',(110.3,-70.3,0.3));
#17572=CARTESIAN_POINT('',(98.5,-70.,0.3));
#17573=CARTESIAN_POINT('Origin',(110.3,-70.3,4.09215166452241));
#17574=CARTESIAN_POINT('',(110.3,-70.,4.09215166452241));
#17575=CARTESIAN_POINT('',(110.,-70.3,4.09215166452241));
#17576=CARTESIAN_POINT('Origin',(110.,-90.,2.78953555269655));
#17577=CARTESIAN_POINT('',(110.,-90.,0.));
#17578=CARTESIAN_POINT('Origin',(87.,-90.,5.39476777634828));
#17579=CARTESIAN_POINT('Origin',(112.,-90.,0.));
#17580=CARTESIAN_POINT('Origin',(112.,-90.,10.7895355526966));
#17581=CARTESIAN_POINT('',(104.475451921837,-84.8,10.7895355526966));
#17582=CARTESIAN_POINT('',(77.8080528673835,-84.8,10.7895355526966));
#17583=CARTESIAN_POINT('',(94.9040264336917,-84.8,10.7895355526966));
#17584=CARTESIAN_POINT('',(77.8080528673835,-75.2,10.7895355526966));
#17585=CARTESIAN_POINT('Origin',(77.8080528673835,-80.,10.7895355526966));
#17586=CARTESIAN_POINT('',(104.475451921837,-75.2,10.7895355526966));
#17587=CARTESIAN_POINT('',(108.237725960918,-75.2,10.7895355526966));
#17588=CARTESIAN_POINT('Origin',(104.475451921837,-80.,10.7895355526966));
#17589=CARTESIAN_POINT('Origin',(70.,-90.,10.7895355526965));
#17590=CARTESIAN_POINT('Origin',(87.,-70.,5.39476777634828));
#17591=CARTESIAN_POINT('Origin',(94.9040264336917,-84.8,10.4895355526966));
#17592=CARTESIAN_POINT('Origin',(77.8080528673835,-84.8,10.4895355526966));
#17593=CARTESIAN_POINT('Origin',(104.475451921837,-84.8,10.4895355526966));
#17594=CARTESIAN_POINT('Origin',(104.475451921837,-80.,10.4895355526966));
#17595=CARTESIAN_POINT('',(104.475451921837,-75.5,10.4895355526966));
#17596=CARTESIAN_POINT('Origin',(104.475451921837,-75.2,10.4895355526966));
#17597=CARTESIAN_POINT('Origin',(104.475451921837,-80.,10.4895355526966));
#17598=CARTESIAN_POINT('Origin',(108.237725960918,-75.2,10.4895355526966));
#17599=CARTESIAN_POINT('Origin',(77.8080528673835,-75.2,10.4895355526966));
#17600=CARTESIAN_POINT('',(108.237725960918,-75.5,10.4895355526966));
#17601=CARTESIAN_POINT('Origin',(77.8080528673835,-80.,10.4895355526966));
#17602=CARTESIAN_POINT('Origin',(104.475451921837,-80.,10.7895355526966));
#17603=CARTESIAN_POINT('',(104.475451921837,-75.5,10.7895355526966));
#17604=CARTESIAN_POINT('Origin',(104.475451921837,-75.5,10.7895355526966));
#17605=CARTESIAN_POINT('Origin',(110.,-90.,0.));
#17822=UNCERTAINTY_MEASURE_WITH_UNIT(LENGTH_MEASURE(0.01),#17837,
'DISTANCE_ACCURACY_VALUE',
'Maximum model space distance between geometric entities at asserted c
onnectivities');
#17824=UNCERTAINTY_MEASURE_WITH_UNIT(LENGTH_MEASURE(0.01),#17837,
'DISTANCE_ACCURACY_VALUE',
'Maximum model space distance between geometric entities at asserted c
onnectivities');
#17834=(
GEOMETRIC_REPRESENTATION_CONTEXT(3)
GLOBAL_UNCERTAINTY_ASSIGNED_CONTEXT((#17822))
GLOBAL_UNIT_ASSIGNED_CONTEXT((#17837,#17839,#17840))
REPRESENTATION_CONTEXT('','3D')
);
#17836=(
GEOMETRIC_REPRESENTATION_CONTEXT(3)
GLOBAL_UNCERTAINTY_ASSIGNED_CONTEXT((#17824))
GLOBAL_UNIT_ASSIGNED_CONTEXT((#17837,#17839,#17840))
REPRESENTATION_CONTEXT('','3D')
);
#17837=(
LENGTH_UNIT()
NAMED_UNIT(*)
SI_UNIT(.MILLI.,.METRE.)
);
#17839=(
NAMED_UNIT(*)
PLANE_ANGLE_UNIT()
SI_UNIT($,.RADIAN.)
);
#17840=(
NAMED_UNIT(*)
SI_UNIT($,.STERADIAN.)
SOLID_ANGLE_UNIT()
);
#17850=SHAPE_DEFINITION_REPRESENTATION(#17861,#17882);
#17861=PRODUCT_DEFINITION_SHAPE('',$,#17894);
#17882=SHAPE_REPRESENTATION('',(#10826),#17834);
#17884=PRODUCT_DEFINITION_CONTEXT('part definition',#17919,'design');
#17894=PRODUCT_DEFINITION('Clamp_03','Clamp_03',#17905,#17884);
#17905=PRODUCT_DEFINITION_FORMATION('',$,#17930);
#17919=APPLICATION_CONTEXT(
'Core Data for Automotive Mechanical Design Process');
#17920=PRODUCT_CONTEXT('part definition',#17919,'mechanical');
#17930=PRODUCT('Clamp_03','Clamp_03',$,(#17920));
#17981=COLOUR_RGB('Off White',0.89,0.88,0.83);
#17982=FILL_AREA_STYLE_COLOUR('',#17981);
#17983=FILL_AREA_STYLE('',(#17982));
#17984=SURFACE_STYLE_FILL_AREA(#17983);
#17985=SURFACE_SIDE_STYLE('',(#17984));
#17986=SURFACE_STYLE_USAGE(.BOTH.,#17985);
#17987=PRESENTATION_STYLE_ASSIGNMENT((#17986));
ENDSEC;
END-ISO-10303-21;
